ISO-10303-21;
HEADER;
/* Generated by software containing ST-Developer
 * from STEP Tools, Inc. (www.steptools.com) 
 */

FILE_DESCRIPTION(
/* description */ (''),
/* implementation_level */ '2;1');

FILE_NAME(
/* name */ 'Middle_Block.step',
/* time_stamp */ '2026-10-19T01:17:59+06:00',
/* author */ (''),
/* organization */ (''),
/* preprocessor_version */ 'ST-DEVELOPER v20.2',
/* originating_system */ 'Autodesk Translation Framework v15.15.0.0',
/* authorisation */ '');

FILE_SCHEMA (('AUTOMOTIVE_DESIGN { 1 0 10303 214 3 1 1 }'));
ENDSEC;

DATA;
#10=MECHANICAL_DESIGN_GEOMETRIC_PRESENTATION_REPRESENTATION('',(#749),#48369);
#618=SHAPE_REPRESENTATION_RELATIONSHIP('SRR','None',#48418,#629);
#629=ADVANCED_BREP_SHAPE_REPRESENTATION('',(#775),#48363);
#688=FACE_BOUND('',#3222,.T.);
#689=FACE_BOUND('',#3245,.T.);
#690=FACE_BOUND('',#3249,.T.);
#691=FACE_BOUND('',#3252,.T.);
#692=FACE_BOUND('',#3253,.T.);
#693=FACE_BOUND('',#3254,.T.);
#694=FACE_BOUND('',#3255,.T.);
#695=FACE_BOUND('',#3256,.T.);
#696=FACE_BOUND('',#3257,.T.);
#697=FACE_BOUND('',#3258,.T.);
#698=FACE_BOUND('',#3259,.T.);
#699=FACE_BOUND('',#3261,.T.);
#700=FACE_BOUND('',#3262,.T.);
#701=FACE_BOUND('',#3263,.T.);
#702=FACE_BOUND('',#3264,.T.);
#703=FACE_BOUND('',#3265,.T.);
#704=FACE_BOUND('',#3266,.T.);
#705=FACE_BOUND('',#3267,.T.);
#706=FACE_BOUND('',#3268,.T.);
#707=FACE_BOUND('',#3274,.T.);
#708=FACE_BOUND('',#3275,.T.);
#709=FACE_BOUND('',#3276,.T.);
#710=FACE_BOUND('',#3277,.T.);
#711=FACE_BOUND('',#3278,.T.);
#712=FACE_BOUND('',#3279,.T.);
#713=FACE_BOUND('',#3280,.T.);
#714=FACE_BOUND('',#3281,.T.);
#715=FACE_BOUND('',#3282,.T.);
#716=FACE_BOUND('',#3283,.T.);
#717=FACE_BOUND('',#3284,.T.);
#718=FACE_BOUND('',#3285,.T.);
#719=FACE_BOUND('',#3286,.T.);
#720=FACE_BOUND('',#3287,.T.);
#721=FACE_BOUND('',#3288,.T.);
#722=FACE_BOUND('',#3289,.T.);
#749=STYLED_ITEM('',(#48496),#775);
#775=MANIFOLD_SOLID_BREP('Middle_Block',#20128);
#1149=CYLINDRICAL_SURFACE('',#21668,3.00000000000001);
#1150=CYLINDRICAL_SURFACE('',#21671,3.00000000000001);
#1151=CYLINDRICAL_SURFACE('',#21674,3.);
#1152=CYLINDRICAL_SURFACE('',#21677,3.);
#1153=CYLINDRICAL_SURFACE('',#21680,3.);
#1154=CYLINDRICAL_SURFACE('',#21683,3.);
#1155=CYLINDRICAL_SURFACE('',#21686,3.00000000000001);
#1156=CYLINDRICAL_SURFACE('',#21689,3.00000000000001);
#1157=CYLINDRICAL_SURFACE('',#21692,3.00000000000001);
#1158=CYLINDRICAL_SURFACE('',#21695,3.00000000000001);
#1159=CYLINDRICAL_SURFACE('',#21698,3.);
#1160=CYLINDRICAL_SURFACE('',#21701,3.);
#1161=CYLINDRICAL_SURFACE('',#21704,3.);
#1162=CYLINDRICAL_SURFACE('',#21707,3.);
#1163=CYLINDRICAL_SURFACE('',#21710,3.00000000000001);
#1164=CYLINDRICAL_SURFACE('',#21713,3.00000000000001);
#1165=CYLINDRICAL_SURFACE('',#21716,8.09375);
#1166=CYLINDRICAL_SURFACE('',#21718,5.);
#1167=CYLINDRICAL_SURFACE('',#21721,5.);
#2124=FACE_OUTER_BOUND('',#3221,.T.);
#2125=FACE_OUTER_BOUND('',#3223,.T.);
#2126=FACE_OUTER_BOUND('',#3224,.T.);
#2127=FACE_OUTER_BOUND('',#3225,.T.);
#2128=FACE_OUTER_BOUND('',#3226,.T.);
#2129=FACE_OUTER_BOUND('',#3227,.T.);
#2130=FACE_OUTER_BOUND('',#3228,.T.);
#2131=FACE_OUTER_BOUND('',#3229,.T.);
#2132=FACE_OUTER_BOUND('',#3230,.T.);
#2133=FACE_OUTER_BOUND('',#3231,.T.);
#2134=FACE_OUTER_BOUND('',#3232,.T.);
#2135=FACE_OUTER_BOUND('',#3233,.T.);
#2136=FACE_OUTER_BOUND('',#3234,.T.);
#2137=FACE_OUTER_BOUND('',#3235,.T.);
#2138=FACE_OUTER_BOUND('',#3236,.T.);
#2139=FACE_OUTER_BOUND('',#3237,.T.);
#2140=FACE_OUTER_BOUND('',#3238,.T.);
#2141=FACE_OUTER_BOUND('',#3239,.T.);
#2142=FACE_OUTER_BOUND('',#3240,.T.);
#2143=FACE_OUTER_BOUND('',#3241,.T.);
#2144=FACE_OUTER_BOUND('',#3242,.T.);
#2145=FACE_OUTER_BOUND('',#3243,.T.);
#2146=FACE_OUTER_BOUND('',#3244,.T.);
#2147=FACE_OUTER_BOUND('',#3246,.T.);
#2148=FACE_OUTER_BOUND('',#3247,.T.);
#2149=FACE_OUTER_BOUND('',#3248,.T.);
#2150=FACE_OUTER_BOUND('',#3250,.T.);
#2151=FACE_OUTER_BOUND('',#3251,.T.);
#2152=FACE_OUTER_BOUND('',#3260,.T.);
#2153=FACE_OUTER_BOUND('',#3269,.T.);
#2154=FACE_OUTER_BOUND('',#3270,.T.);
#2155=FACE_OUTER_BOUND('',#3271,.T.);
#2156=FACE_OUTER_BOUND('',#3272,.T.);
#2157=FACE_OUTER_BOUND('',#3273,.T.);
#3221=EDGE_LOOP('',(#17851,#17852,#17853,#17854,#17855,#17856));
#3222=EDGE_LOOP('',(#17857));
#3223=EDGE_LOOP('',(#17858,#17859,#17860,#17861));
#3224=EDGE_LOOP('',(#17862,#17863,#17864,#17865));
#3225=EDGE_LOOP('',(#17866,#17867,#17868,#17869));
#3226=EDGE_LOOP('',(#17870,#17871,#17872,#17873));
#3227=EDGE_LOOP('',(#17874,#17875,#17876,#17877));
#3228=EDGE_LOOP('',(#17878,#17879,#17880,#17881));
#3229=EDGE_LOOP('',(#17882,#17883,#17884,#17885));
#3230=EDGE_LOOP('',(#17886,#17887,#17888,#17889));
#3231=EDGE_LOOP('',(#17890,#17891,#17892,#17893));
#3232=EDGE_LOOP('',(#17894,#17895,#17896,#17897));
#3233=EDGE_LOOP('',(#17898,#17899,#17900,#17901));
#3234=EDGE_LOOP('',(#17902,#17903,#17904,#17905));
#3235=EDGE_LOOP('',(#17906,#17907,#17908,#17909));
#3236=EDGE_LOOP('',(#17910,#17911,#17912,#17913));
#3237=EDGE_LOOP('',(#17914,#17915,#17916,#17917));
#3238=EDGE_LOOP('',(#17918,#17919,#17920,#17921));
#3239=EDGE_LOOP('',(#17922,#17923,#17924,#17925));
#3240=EDGE_LOOP('',(#17926,#17927,#17928,#17929));
#3241=EDGE_LOOP('',(#17930,#17931,#17932,#17933));
#3242=EDGE_LOOP('',(#17934,#17935,#17936,#17937));
#3243=EDGE_LOOP('',(#17938,#17939,#17940,#17941));
#3244=EDGE_LOOP('',(#17942,#17943,#17944,#17945,#17946,#17947));
#3245=EDGE_LOOP('',(#17948));
#3246=EDGE_LOOP('',(#17949,#17950,#17951,#17952));
#3247=EDGE_LOOP('',(#17953,#17954,#17955,#17956));
#3248=EDGE_LOOP('',(#17957,#17958,#17959,#17960));
#3249=EDGE_LOOP('',(#17961,#17962,#17963,#17964));
#3250=EDGE_LOOP('',(#17965,#17966,#17967,#17968));
#3251=EDGE_LOOP('',(#17969,#17970,#17971,#17972));
#3252=EDGE_LOOP('',(#17973));
#3253=EDGE_LOOP('',(#17974));
#3254=EDGE_LOOP('',(#17975));
#3255=EDGE_LOOP('',(#17976));
#3256=EDGE_LOOP('',(#17977));
#3257=EDGE_LOOP('',(#17978));
#3258=EDGE_LOOP('',(#17979));
#3259=EDGE_LOOP('',(#17980));
#3260=EDGE_LOOP('',(#17981,#17982,#17983,#17984));
#3261=EDGE_LOOP('',(#17985));
#3262=EDGE_LOOP('',(#17986));
#3263=EDGE_LOOP('',(#17987));
#3264=EDGE_LOOP('',(#17988));
#3265=EDGE_LOOP('',(#17989));
#3266=EDGE_LOOP('',(#17990));
#3267=EDGE_LOOP('',(#17991));
#3268=EDGE_LOOP('',(#17992));
#3269=EDGE_LOOP('',(#17993,#17994,#17995,#17996,#17997,#17998,#17999,#18000));
#3270=EDGE_LOOP('',(#18001,#18002,#18003,#18004,#18005,#18006,#18007,#18008));
#3271=EDGE_LOOP('',(#18009,#18010,#18011,#18012));
#3272=EDGE_LOOP('',(#18013,#18014,#18015,#18016));
#3273=EDGE_LOOP('',(#18017,#18018,#18019,#18020));
#3274=EDGE_LOOP('',(#18021));
#3275=EDGE_LOOP('',(#18022));
#3276=EDGE_LOOP('',(#18023));
#3277=EDGE_LOOP('',(#18024));
#3278=EDGE_LOOP('',(#18025));
#3279=EDGE_LOOP('',(#18026));
#3280=EDGE_LOOP('',(#18027));
#3281=EDGE_LOOP('',(#18028));
#3282=EDGE_LOOP('',(#18029));
#3283=EDGE_LOOP('',(#18030));
#3284=EDGE_LOOP('',(#18031));
#3285=EDGE_LOOP('',(#18032));
#3286=EDGE_LOOP('',(#18033));
#3287=EDGE_LOOP('',(#18034));
#3288=EDGE_LOOP('',(#18035));
#3289=EDGE_LOOP('',(#18036));
#3877=CIRCLE('',#21665,5.);
#3878=CIRCLE('',#21666,5.);
#3879=CIRCLE('',#21667,8.09375);
#3880=CIRCLE('',#21669,3.00000000000001);
#3881=CIRCLE('',#21670,3.00000000000001);
#3882=CIRCLE('',#21672,3.00000000000001);
#3883=CIRCLE('',#21673,3.00000000000001);
#3884=CIRCLE('',#21675,3.);
#3885=CIRCLE('',#21676,3.);
#3886=CIRCLE('',#21678,3.);
#3887=CIRCLE('',#21679,3.);
#3888=CIRCLE('',#21681,3.);
#3889=CIRCLE('',#21682,3.);
#3890=CIRCLE('',#21684,3.);
#3891=CIRCLE('',#21685,3.);
#3892=CIRCLE('',#21687,3.00000000000001);
#3893=CIRCLE('',#21688,3.00000000000001);
#3894=CIRCLE('',#21690,3.00000000000001);
#3895=CIRCLE('',#21691,3.00000000000001);
#3896=CIRCLE('',#21693,3.00000000000001);
#3897=CIRCLE('',#21694,3.00000000000001);
#3898=CIRCLE('',#21696,3.00000000000001);
#3899=CIRCLE('',#21697,3.00000000000001);
#3900=CIRCLE('',#21699,3.);
#3901=CIRCLE('',#21700,3.);
#3902=CIRCLE('',#21702,3.);
#3903=CIRCLE('',#21703,3.);
#3904=CIRCLE('',#21705,3.);
#3905=CIRCLE('',#21706,3.);
#3906=CIRCLE('',#21708,3.);
#3907=CIRCLE('',#21709,3.);
#3908=CIRCLE('',#21711,3.00000000000001);
#3909=CIRCLE('',#21712,3.00000000000001);
#3910=CIRCLE('',#21714,3.00000000000001);
#3911=CIRCLE('',#21715,3.00000000000001);
#3912=CIRCLE('',#21717,8.09375);
#3913=CIRCLE('',#21719,5.);
#3914=CIRCLE('',#21722,5.);
#5648=LINE('',#47633,#7529);
#5649=LINE('',#47637,#7530);
#5650=LINE('',#47639,#7531);
#5651=LINE('',#47640,#7532);
#5652=LINE('',#47647,#7533);
#5653=LINE('',#47653,#7534);
#5654=LINE('',#47659,#7535);
#5655=LINE('',#47665,#7536);
#5656=LINE('',#47671,#7537);
#5657=LINE('',#47677,#7538);
#5658=LINE('',#47683,#7539);
#5659=LINE('',#47689,#7540);
#5660=LINE('',#47695,#7541);
#5661=LINE('',#47701,#7542);
#5662=LINE('',#47707,#7543);
#5663=LINE('',#47713,#7544);
#5664=LINE('',#47719,#7545);
#5665=LINE('',#47725,#7546);
#5666=LINE('',#47731,#7547);
#5667=LINE('',#47737,#7548);
#5668=LINE('',#47742,#7549);
#5669=LINE('',#47747,#7550);
#5670=LINE('',#47748,#7551);
#5671=LINE('',#47751,#7552);
#5672=LINE('',#47752,#7553);
#5673=LINE('',#47756,#7554);
#5674=LINE('',#47759,#7555);
#5675=LINE('',#47760,#7556);
#5676=LINE('',#47763,#7557);
#5677=LINE('',#47764,#7558);
#5678=LINE('',#47766,#7559);
#5679=LINE('',#47770,#7560);
#5680=LINE('',#47772,#7561);
#5681=LINE('',#47774,#7562);
#5682=LINE('',#47775,#7563);
#5683=LINE('',#47778,#7564);
#5684=LINE('',#47780,#7565);
#5685=LINE('',#47781,#7566);
#5686=LINE('',#47784,#7567);
#5687=LINE('',#47786,#7568);
#5688=LINE('',#47787,#7569);
#5689=LINE('',#47790,#7570);
#5690=LINE('',#47792,#7571);
#5691=LINE('',#47793,#7572);
#5692=LINE('',#47796,#7573);
#5693=LINE('',#47798,#7574);
#5694=LINE('',#47799,#7575);
#5695=LINE('',#47802,#7576);
#5696=LINE('',#47804,#7577);
#5697=LINE('',#47805,#7578);
#5698=LINE('',#47808,#7579);
#5699=LINE('',#47810,#7580);
#5700=LINE('',#47811,#7581);
#5701=LINE('',#47813,#7582);
#5702=LINE('',#47815,#7583);
#7529=VECTOR('',#26401,10.);
#7530=VECTOR('',#26404,10.);
#7531=VECTOR('',#26405,10.);
#7532=VECTOR('',#26406,10.);
#7533=VECTOR('',#26413,3.00000000000001);
#7534=VECTOR('',#26420,3.00000000000001);
#7535=VECTOR('',#26427,3.);
#7536=VECTOR('',#26434,3.);
#7537=VECTOR('',#26441,3.);
#7538=VECTOR('',#26448,3.);
#7539=VECTOR('',#26455,3.00000000000001);
#7540=VECTOR('',#26462,3.00000000000001);
#7541=VECTOR('',#26469,3.00000000000001);
#7542=VECTOR('',#26476,3.00000000000001);
#7543=VECTOR('',#26483,3.);
#7544=VECTOR('',#26490,3.);
#7545=VECTOR('',#26497,3.);
#7546=VECTOR('',#26504,3.);
#7547=VECTOR('',#26511,3.00000000000001);
#7548=VECTOR('',#26518,3.00000000000001);
#7549=VECTOR('',#26525,8.25000000000001);
#7550=VECTOR('',#26530,10.);
#7551=VECTOR('',#26531,10.);
#7552=VECTOR('',#26534,10.);
#7553=VECTOR('',#26535,10.);
#7554=VECTOR('',#26540,10.);
#7555=VECTOR('',#26543,10.);
#7556=VECTOR('',#26544,10.);
#7557=VECTOR('',#26547,10.);
#7558=VECTOR('',#26548,10.);
#7559=VECTOR('',#26551,10.);
#7560=VECTOR('',#26554,10.);
#7561=VECTOR('',#26555,10.);
#7562=VECTOR('',#26556,10.);
#7563=VECTOR('',#26557,10.);
#7564=VECTOR('',#26560,10.);
#7565=VECTOR('',#26561,10.);
#7566=VECTOR('',#26562,10.);
#7567=VECTOR('',#26565,10.);
#7568=VECTOR('',#26566,10.);
#7569=VECTOR('',#26567,10.);
#7570=VECTOR('',#26570,10.);
#7571=VECTOR('',#26571,10.);
#7572=VECTOR('',#26572,10.);
#7573=VECTOR('',#26575,10.);
#7574=VECTOR('',#26576,10.);
#7575=VECTOR('',#26577,10.);
#7576=VECTOR('',#26580,10.);
#7577=VECTOR('',#26581,10.);
#7578=VECTOR('',#26582,10.);
#7579=VECTOR('',#26585,10.);
#7580=VECTOR('',#26586,10.);
#7581=VECTOR('',#26587,10.);
#7582=VECTOR('',#26590,10.);
#7583=VECTOR('',#26593,10.);
#9481=VERTEX_POINT('',#47629);
#9482=VERTEX_POINT('',#47630);
#9483=VERTEX_POINT('',#47632);
#9484=VERTEX_POINT('',#47634);
#9485=VERTEX_POINT('',#47636);
#9486=VERTEX_POINT('',#47638);
#9487=VERTEX_POINT('',#47641);
#9488=VERTEX_POINT('',#47644);
#9489=VERTEX_POINT('',#47646);
#9490=VERTEX_POINT('',#47650);
#9491=VERTEX_POINT('',#47652);
#9492=VERTEX_POINT('',#47656);
#9493=VERTEX_POINT('',#47658);
#9494=VERTEX_POINT('',#47662);
#9495=VERTEX_POINT('',#47664);
#9496=VERTEX_POINT('',#47668);
#9497=VERTEX_POINT('',#47670);
#9498=VERTEX_POINT('',#47674);
#9499=VERTEX_POINT('',#47676);
#9500=VERTEX_POINT('',#47680);
#9501=VERTEX_POINT('',#47682);
#9502=VERTEX_POINT('',#47686);
#9503=VERTEX_POINT('',#47688);
#9504=VERTEX_POINT('',#47692);
#9505=VERTEX_POINT('',#47694);
#9506=VERTEX_POINT('',#47698);
#9507=VERTEX_POINT('',#47700);
#9508=VERTEX_POINT('',#47704);
#9509=VERTEX_POINT('',#47706);
#9510=VERTEX_POINT('',#47710);
#9511=VERTEX_POINT('',#47712);
#9512=VERTEX_POINT('',#47716);
#9513=VERTEX_POINT('',#47718);
#9514=VERTEX_POINT('',#47722);
#9515=VERTEX_POINT('',#47724);
#9516=VERTEX_POINT('',#47728);
#9517=VERTEX_POINT('',#47730);
#9518=VERTEX_POINT('',#47734);
#9519=VERTEX_POINT('',#47736);
#9520=VERTEX_POINT('',#47740);
#9521=VERTEX_POINT('',#47744);
#9522=VERTEX_POINT('',#47745);
#9523=VERTEX_POINT('',#47750);
#9524=VERTEX_POINT('',#47754);
#9525=VERTEX_POINT('',#47758);
#9526=VERTEX_POINT('',#47762);
#9527=VERTEX_POINT('',#47768);
#9528=VERTEX_POINT('',#47769);
#9529=VERTEX_POINT('',#47771);
#9530=VERTEX_POINT('',#47773);
#9531=VERTEX_POINT('',#47777);
#9532=VERTEX_POINT('',#47779);
#9533=VERTEX_POINT('',#47783);
#9534=VERTEX_POINT('',#47785);
#9535=VERTEX_POINT('',#47789);
#9536=VERTEX_POINT('',#47791);
#9537=VERTEX_POINT('',#47795);
#9538=VERTEX_POINT('',#47797);
#9539=VERTEX_POINT('',#47801);
#9540=VERTEX_POINT('',#47803);
#9541=VERTEX_POINT('',#47807);
#9542=VERTEX_POINT('',#47809);
#12309=EDGE_CURVE('',#9481,#9482,#3877,.T.);
#12310=EDGE_CURVE('',#9483,#9481,#5648,.T.);
#12311=EDGE_CURVE('',#9484,#9483,#3878,.T.);
#12312=EDGE_CURVE('',#9485,#9484,#5649,.T.);
#12313=EDGE_CURVE('',#9486,#9485,#5650,.T.);
#12314=EDGE_CURVE('',#9486,#9482,#5651,.T.);
#12315=EDGE_CURVE('',#9487,#9487,#3879,.T.);
#12316=EDGE_CURVE('',#9488,#9488,#3880,.T.);
#12317=EDGE_CURVE('',#9488,#9489,#5652,.T.);
#12318=EDGE_CURVE('',#9489,#9489,#3881,.T.);
#12319=EDGE_CURVE('',#9490,#9490,#3882,.T.);
#12320=EDGE_CURVE('',#9490,#9491,#5653,.T.);
#12321=EDGE_CURVE('',#9491,#9491,#3883,.T.);
#12322=EDGE_CURVE('',#9492,#9492,#3884,.T.);
#12323=EDGE_CURVE('',#9492,#9493,#5654,.T.);
#12324=EDGE_CURVE('',#9493,#9493,#3885,.T.);
#12325=EDGE_CURVE('',#9494,#9494,#3886,.T.);
#12326=EDGE_CURVE('',#9494,#9495,#5655,.T.);
#12327=EDGE_CURVE('',#9495,#9495,#3887,.T.);
#12328=EDGE_CURVE('',#9496,#9496,#3888,.T.);
#12329=EDGE_CURVE('',#9496,#9497,#5656,.T.);
#12330=EDGE_CURVE('',#9497,#9497,#3889,.T.);
#12331=EDGE_CURVE('',#9498,#9498,#3890,.T.);
#12332=EDGE_CURVE('',#9498,#9499,#5657,.T.);
#12333=EDGE_CURVE('',#9499,#9499,#3891,.T.);
#12334=EDGE_CURVE('',#9500,#9500,#3892,.T.);
#12335=EDGE_CURVE('',#9500,#9501,#5658,.T.);
#12336=EDGE_CURVE('',#9501,#9501,#3893,.T.);
#12337=EDGE_CURVE('',#9502,#9502,#3894,.T.);
#12338=EDGE_CURVE('',#9502,#9503,#5659,.T.);
#12339=EDGE_CURVE('',#9503,#9503,#3895,.T.);
#12340=EDGE_CURVE('',#9504,#9504,#3896,.T.);
#12341=EDGE_CURVE('',#9504,#9505,#5660,.T.);
#12342=EDGE_CURVE('',#9505,#9505,#3897,.T.);
#12343=EDGE_CURVE('',#9506,#9506,#3898,.T.);
#12344=EDGE_CURVE('',#9506,#9507,#5661,.T.);
#12345=EDGE_CURVE('',#9507,#9507,#3899,.T.);
#12346=EDGE_CURVE('',#9508,#9508,#3900,.T.);
#12347=EDGE_CURVE('',#9508,#9509,#5662,.T.);
#12348=EDGE_CURVE('',#9509,#9509,#3901,.T.);
#12349=EDGE_CURVE('',#9510,#9510,#3902,.T.);
#12350=EDGE_CURVE('',#9510,#9511,#5663,.T.);
#12351=EDGE_CURVE('',#9511,#9511,#3903,.T.);
#12352=EDGE_CURVE('',#9512,#9512,#3904,.T.);
#12353=EDGE_CURVE('',#9512,#9513,#5664,.T.);
#12354=EDGE_CURVE('',#9513,#9513,#3905,.T.);
#12355=EDGE_CURVE('',#9514,#9514,#3906,.T.);
#12356=EDGE_CURVE('',#9514,#9515,#5665,.T.);
#12357=EDGE_CURVE('',#9515,#9515,#3907,.T.);
#12358=EDGE_CURVE('',#9516,#9516,#3908,.T.);
#12359=EDGE_CURVE('',#9516,#9517,#5666,.T.);
#12360=EDGE_CURVE('',#9517,#9517,#3909,.T.);
#12361=EDGE_CURVE('',#9518,#9518,#3910,.T.);
#12362=EDGE_CURVE('',#9518,#9519,#5667,.T.);
#12363=EDGE_CURVE('',#9519,#9519,#3911,.T.);
#12364=EDGE_CURVE('',#9520,#9520,#3912,.T.);
#12365=EDGE_CURVE('',#9520,#9487,#5668,.T.);
#12366=EDGE_CURVE('',#9521,#9522,#3913,.T.);
#12367=EDGE_CURVE('',#9522,#9481,#5669,.T.);
#12368=EDGE_CURVE('',#9482,#9521,#5670,.T.);
#12369=EDGE_CURVE('',#9522,#9523,#5671,.T.);
#12370=EDGE_CURVE('',#9483,#9523,#5672,.T.);
#12371=EDGE_CURVE('',#9523,#9524,#3914,.T.);
#12372=EDGE_CURVE('',#9524,#9484,#5673,.T.);
#12373=EDGE_CURVE('',#9525,#9524,#5674,.T.);
#12374=EDGE_CURVE('',#9485,#9525,#5675,.T.);
#12375=EDGE_CURVE('',#9526,#9521,#5676,.T.);
#12376=EDGE_CURVE('',#9525,#9526,#5677,.T.);
#12377=EDGE_CURVE('',#9526,#9486,#5678,.T.);
#12378=EDGE_CURVE('',#9527,#9528,#5679,.T.);
#12379=EDGE_CURVE('',#9527,#9529,#5680,.T.);
#12380=EDGE_CURVE('',#9530,#9529,#5681,.T.);
#12381=EDGE_CURVE('',#9528,#9530,#5682,.T.);
#12382=EDGE_CURVE('',#9531,#9527,#5683,.T.);
#12383=EDGE_CURVE('',#9531,#9532,#5684,.T.);
#12384=EDGE_CURVE('',#9529,#9532,#5685,.T.);
#12385=EDGE_CURVE('',#9533,#9531,#5686,.T.);
#12386=EDGE_CURVE('',#9534,#9533,#5687,.T.);
#12387=EDGE_CURVE('',#9532,#9534,#5688,.T.);
#12388=EDGE_CURVE('',#9535,#9530,#5689,.T.);
#12389=EDGE_CURVE('',#9536,#9535,#5690,.T.);
#12390=EDGE_CURVE('',#9528,#9536,#5691,.T.);
#12391=EDGE_CURVE('',#9537,#9533,#5692,.T.);
#12392=EDGE_CURVE('',#9538,#9537,#5693,.T.);
#12393=EDGE_CURVE('',#9534,#9538,#5694,.T.);
#12394=EDGE_CURVE('',#9536,#9539,#5695,.T.);
#12395=EDGE_CURVE('',#9540,#9539,#5696,.T.);
#12396=EDGE_CURVE('',#9537,#9540,#5697,.T.);
#12397=EDGE_CURVE('',#9538,#9541,#5698,.T.);
#12398=EDGE_CURVE('',#9542,#9541,#5699,.T.);
#12399=EDGE_CURVE('',#9535,#9542,#5700,.T.);
#12400=EDGE_CURVE('',#9539,#9542,#5701,.T.);
#12401=EDGE_CURVE('',#9541,#9540,#5702,.T.);
#17851=ORIENTED_EDGE('',*,*,#12309,.F.);
#17852=ORIENTED_EDGE('',*,*,#12310,.F.);
#17853=ORIENTED_EDGE('',*,*,#12311,.F.);
#17854=ORIENTED_EDGE('',*,*,#12312,.F.);
#17855=ORIENTED_EDGE('',*,*,#12313,.F.);
#17856=ORIENTED_EDGE('',*,*,#12314,.T.);
#17857=ORIENTED_EDGE('',*,*,#12315,.T.);
#17858=ORIENTED_EDGE('',*,*,#12316,.F.);
#17859=ORIENTED_EDGE('',*,*,#12317,.T.);
#17860=ORIENTED_EDGE('',*,*,#12318,.F.);
#17861=ORIENTED_EDGE('',*,*,#12317,.F.);
#17862=ORIENTED_EDGE('',*,*,#12319,.F.);
#17863=ORIENTED_EDGE('',*,*,#12320,.T.);
#17864=ORIENTED_EDGE('',*,*,#12321,.F.);
#17865=ORIENTED_EDGE('',*,*,#12320,.F.);
#17866=ORIENTED_EDGE('',*,*,#12322,.F.);
#17867=ORIENTED_EDGE('',*,*,#12323,.T.);
#17868=ORIENTED_EDGE('',*,*,#12324,.F.);
#17869=ORIENTED_EDGE('',*,*,#12323,.F.);
#17870=ORIENTED_EDGE('',*,*,#12325,.F.);
#17871=ORIENTED_EDGE('',*,*,#12326,.T.);
#17872=ORIENTED_EDGE('',*,*,#12327,.F.);
#17873=ORIENTED_EDGE('',*,*,#12326,.F.);
#17874=ORIENTED_EDGE('',*,*,#12328,.F.);
#17875=ORIENTED_EDGE('',*,*,#12329,.T.);
#17876=ORIENTED_EDGE('',*,*,#12330,.F.);
#17877=ORIENTED_EDGE('',*,*,#12329,.F.);
#17878=ORIENTED_EDGE('',*,*,#12331,.F.);
#17879=ORIENTED_EDGE('',*,*,#12332,.T.);
#17880=ORIENTED_EDGE('',*,*,#12333,.F.);
#17881=ORIENTED_EDGE('',*,*,#12332,.F.);
#17882=ORIENTED_EDGE('',*,*,#12334,.F.);
#17883=ORIENTED_EDGE('',*,*,#12335,.T.);
#17884=ORIENTED_EDGE('',*,*,#12336,.F.);
#17885=ORIENTED_EDGE('',*,*,#12335,.F.);
#17886=ORIENTED_EDGE('',*,*,#12337,.F.);
#17887=ORIENTED_EDGE('',*,*,#12338,.T.);
#17888=ORIENTED_EDGE('',*,*,#12339,.F.);
#17889=ORIENTED_EDGE('',*,*,#12338,.F.);
#17890=ORIENTED_EDGE('',*,*,#12340,.F.);
#17891=ORIENTED_EDGE('',*,*,#12341,.T.);
#17892=ORIENTED_EDGE('',*,*,#12342,.F.);
#17893=ORIENTED_EDGE('',*,*,#12341,.F.);
#17894=ORIENTED_EDGE('',*,*,#12343,.F.);
#17895=ORIENTED_EDGE('',*,*,#12344,.T.);
#17896=ORIENTED_EDGE('',*,*,#12345,.F.);
#17897=ORIENTED_EDGE('',*,*,#12344,.F.);
#17898=ORIENTED_EDGE('',*,*,#12346,.F.);
#17899=ORIENTED_EDGE('',*,*,#12347,.T.);
#17900=ORIENTED_EDGE('',*,*,#12348,.F.);
#17901=ORIENTED_EDGE('',*,*,#12347,.F.);
#17902=ORIENTED_EDGE('',*,*,#12349,.F.);
#17903=ORIENTED_EDGE('',*,*,#12350,.T.);
#17904=ORIENTED_EDGE('',*,*,#12351,.F.);
#17905=ORIENTED_EDGE('',*,*,#12350,.F.);
#17906=ORIENTED_EDGE('',*,*,#12352,.F.);
#17907=ORIENTED_EDGE('',*,*,#12353,.T.);
#17908=ORIENTED_EDGE('',*,*,#12354,.F.);
#17909=ORIENTED_EDGE('',*,*,#12353,.F.);
#17910=ORIENTED_EDGE('',*,*,#12355,.F.);
#17911=ORIENTED_EDGE('',*,*,#12356,.T.);
#17912=ORIENTED_EDGE('',*,*,#12357,.F.);
#17913=ORIENTED_EDGE('',*,*,#12356,.F.);
#17914=ORIENTED_EDGE('',*,*,#12358,.F.);
#17915=ORIENTED_EDGE('',*,*,#12359,.T.);
#17916=ORIENTED_EDGE('',*,*,#12360,.F.);
#17917=ORIENTED_EDGE('',*,*,#12359,.F.);
#17918=ORIENTED_EDGE('',*,*,#12361,.F.);
#17919=ORIENTED_EDGE('',*,*,#12362,.T.);
#17920=ORIENTED_EDGE('',*,*,#12363,.F.);
#17921=ORIENTED_EDGE('',*,*,#12362,.F.);
#17922=ORIENTED_EDGE('',*,*,#12364,.F.);
#17923=ORIENTED_EDGE('',*,*,#12365,.T.);
#17924=ORIENTED_EDGE('',*,*,#12315,.F.);
#17925=ORIENTED_EDGE('',*,*,#12365,.F.);
#17926=ORIENTED_EDGE('',*,*,#12366,.T.);
#17927=ORIENTED_EDGE('',*,*,#12367,.T.);
#17928=ORIENTED_EDGE('',*,*,#12309,.T.);
#17929=ORIENTED_EDGE('',*,*,#12368,.T.);
#17930=ORIENTED_EDGE('',*,*,#12367,.F.);
#17931=ORIENTED_EDGE('',*,*,#12369,.T.);
#17932=ORIENTED_EDGE('',*,*,#12370,.F.);
#17933=ORIENTED_EDGE('',*,*,#12310,.T.);
#17934=ORIENTED_EDGE('',*,*,#12311,.T.);
#17935=ORIENTED_EDGE('',*,*,#12370,.T.);
#17936=ORIENTED_EDGE('',*,*,#12371,.T.);
#17937=ORIENTED_EDGE('',*,*,#12372,.T.);
#17938=ORIENTED_EDGE('',*,*,#12372,.F.);
#17939=ORIENTED_EDGE('',*,*,#12373,.F.);
#17940=ORIENTED_EDGE('',*,*,#12374,.F.);
#17941=ORIENTED_EDGE('',*,*,#12312,.T.);
#17942=ORIENTED_EDGE('',*,*,#12366,.F.);
#17943=ORIENTED_EDGE('',*,*,#12375,.F.);
#17944=ORIENTED_EDGE('',*,*,#12376,.F.);
#17945=ORIENTED_EDGE('',*,*,#12373,.T.);
#17946=ORIENTED_EDGE('',*,*,#12371,.F.);
#17947=ORIENTED_EDGE('',*,*,#12369,.F.);
#17948=ORIENTED_EDGE('',*,*,#12364,.T.);
#17949=ORIENTED_EDGE('',*,*,#12368,.F.);
#17950=ORIENTED_EDGE('',*,*,#12314,.F.);
#17951=ORIENTED_EDGE('',*,*,#12377,.F.);
#17952=ORIENTED_EDGE('',*,*,#12375,.T.);
#17953=ORIENTED_EDGE('',*,*,#12378,.F.);
#17954=ORIENTED_EDGE('',*,*,#12379,.T.);
#17955=ORIENTED_EDGE('',*,*,#12380,.F.);
#17956=ORIENTED_EDGE('',*,*,#12381,.F.);
#17957=ORIENTED_EDGE('',*,*,#12382,.F.);
#17958=ORIENTED_EDGE('',*,*,#12383,.T.);
#17959=ORIENTED_EDGE('',*,*,#12384,.F.);
#17960=ORIENTED_EDGE('',*,*,#12379,.F.);
#17961=ORIENTED_EDGE('',*,*,#12313,.T.);
#17962=ORIENTED_EDGE('',*,*,#12374,.T.);
#17963=ORIENTED_EDGE('',*,*,#12376,.T.);
#17964=ORIENTED_EDGE('',*,*,#12377,.T.);
#17965=ORIENTED_EDGE('',*,*,#12385,.F.);
#17966=ORIENTED_EDGE('',*,*,#12386,.F.);
#17967=ORIENTED_EDGE('',*,*,#12387,.F.);
#17968=ORIENTED_EDGE('',*,*,#12383,.F.);
#17969=ORIENTED_EDGE('',*,*,#12381,.T.);
#17970=ORIENTED_EDGE('',*,*,#12388,.F.);
#17971=ORIENTED_EDGE('',*,*,#12389,.F.);
#17972=ORIENTED_EDGE('',*,*,#12390,.F.);
#17973=ORIENTED_EDGE('',*,*,#12363,.T.);
#17974=ORIENTED_EDGE('',*,*,#12360,.T.);
#17975=ORIENTED_EDGE('',*,*,#12345,.T.);
#17976=ORIENTED_EDGE('',*,*,#12342,.T.);
#17977=ORIENTED_EDGE('',*,*,#12339,.T.);
#17978=ORIENTED_EDGE('',*,*,#12336,.T.);
#17979=ORIENTED_EDGE('',*,*,#12321,.T.);
#17980=ORIENTED_EDGE('',*,*,#12318,.T.);
#17981=ORIENTED_EDGE('',*,*,#12386,.T.);
#17982=ORIENTED_EDGE('',*,*,#12391,.F.);
#17983=ORIENTED_EDGE('',*,*,#12392,.F.);
#17984=ORIENTED_EDGE('',*,*,#12393,.F.);
#17985=ORIENTED_EDGE('',*,*,#12357,.T.);
#17986=ORIENTED_EDGE('',*,*,#12354,.T.);
#17987=ORIENTED_EDGE('',*,*,#12351,.T.);
#17988=ORIENTED_EDGE('',*,*,#12348,.T.);
#17989=ORIENTED_EDGE('',*,*,#12333,.T.);
#17990=ORIENTED_EDGE('',*,*,#12330,.T.);
#17991=ORIENTED_EDGE('',*,*,#12327,.T.);
#17992=ORIENTED_EDGE('',*,*,#12324,.T.);
#17993=ORIENTED_EDGE('',*,*,#12385,.T.);
#17994=ORIENTED_EDGE('',*,*,#12382,.T.);
#17995=ORIENTED_EDGE('',*,*,#12378,.T.);
#17996=ORIENTED_EDGE('',*,*,#12390,.T.);
#17997=ORIENTED_EDGE('',*,*,#12394,.T.);
#17998=ORIENTED_EDGE('',*,*,#12395,.F.);
#17999=ORIENTED_EDGE('',*,*,#12396,.F.);
#18000=ORIENTED_EDGE('',*,*,#12391,.T.);
#18001=ORIENTED_EDGE('',*,*,#12387,.T.);
#18002=ORIENTED_EDGE('',*,*,#12393,.T.);
#18003=ORIENTED_EDGE('',*,*,#12397,.T.);
#18004=ORIENTED_EDGE('',*,*,#12398,.F.);
#18005=ORIENTED_EDGE('',*,*,#12399,.F.);
#18006=ORIENTED_EDGE('',*,*,#12388,.T.);
#18007=ORIENTED_EDGE('',*,*,#12380,.T.);
#18008=ORIENTED_EDGE('',*,*,#12384,.T.);
#18009=ORIENTED_EDGE('',*,*,#12389,.T.);
#18010=ORIENTED_EDGE('',*,*,#12399,.T.);
#18011=ORIENTED_EDGE('',*,*,#12400,.F.);
#18012=ORIENTED_EDGE('',*,*,#12394,.F.);
#18013=ORIENTED_EDGE('',*,*,#12392,.T.);
#18014=ORIENTED_EDGE('',*,*,#12396,.T.);
#18015=ORIENTED_EDGE('',*,*,#12401,.F.);
#18016=ORIENTED_EDGE('',*,*,#12397,.F.);
#18017=ORIENTED_EDGE('',*,*,#12401,.T.);
#18018=ORIENTED_EDGE('',*,*,#12395,.T.);
#18019=ORIENTED_EDGE('',*,*,#12400,.T.);
#18020=ORIENTED_EDGE('',*,*,#12398,.T.);
#18021=ORIENTED_EDGE('',*,*,#12361,.T.);
#18022=ORIENTED_EDGE('',*,*,#12358,.T.);
#18023=ORIENTED_EDGE('',*,*,#12355,.T.);
#18024=ORIENTED_EDGE('',*,*,#12352,.T.);
#18025=ORIENTED_EDGE('',*,*,#12349,.T.);
#18026=ORIENTED_EDGE('',*,*,#12346,.T.);
#18027=ORIENTED_EDGE('',*,*,#12343,.T.);
#18028=ORIENTED_EDGE('',*,*,#12340,.T.);
#18029=ORIENTED_EDGE('',*,*,#12337,.T.);
#18030=ORIENTED_EDGE('',*,*,#12334,.T.);
#18031=ORIENTED_EDGE('',*,*,#12331,.T.);
#18032=ORIENTED_EDGE('',*,*,#12328,.T.);
#18033=ORIENTED_EDGE('',*,*,#12325,.T.);
#18034=ORIENTED_EDGE('',*,*,#12322,.T.);
#18035=ORIENTED_EDGE('',*,*,#12319,.T.);
#18036=ORIENTED_EDGE('',*,*,#12316,.T.);
#18995=PLANE('',#21664);
#18996=PLANE('',#21720);
#18997=PLANE('',#21723);
#18998=PLANE('',#21724);
#18999=PLANE('',#21725);
#19000=PLANE('',#21726);
#19001=PLANE('',#21727);
#19002=PLANE('',#21728);
#19003=PLANE('',#21729);
#19004=PLANE('',#21730);
#19005=PLANE('',#21731);
#19006=PLANE('',#21732);
#19007=PLANE('',#21733);
#19008=PLANE('',#21734);
#19009=PLANE('',#21735);
#19981=ADVANCED_FACE('',(#2124,#688),#18995,.T.);
#19982=ADVANCED_FACE('',(#2125),#1149,.F.);
#19983=ADVANCED_FACE('',(#2126),#1150,.F.);
#19984=ADVANCED_FACE('',(#2127),#1151,.F.);
#19985=ADVANCED_FACE('',(#2128),#1152,.F.);
#19986=ADVANCED_FACE('',(#2129),#1153,.F.);
#19987=ADVANCED_FACE('',(#2130),#1154,.F.);
#19988=ADVANCED_FACE('',(#2131),#1155,.F.);
#19989=ADVANCED_FACE('',(#2132),#1156,.F.);
#19990=ADVANCED_FACE('',(#2133),#1157,.F.);
#19991=ADVANCED_FACE('',(#2134),#1158,.F.);
#19992=ADVANCED_FACE('',(#2135),#1159,.F.);
#19993=ADVANCED_FACE('',(#2136),#1160,.F.);
#19994=ADVANCED_FACE('',(#2137),#1161,.F.);
#19995=ADVANCED_FACE('',(#2138),#1162,.F.);
#19996=ADVANCED_FACE('',(#2139),#1163,.F.);
#19997=ADVANCED_FACE('',(#2140),#1164,.F.);
#19998=ADVANCED_FACE('',(#2141),#1165,.F.);
#19999=ADVANCED_FACE('',(#2142),#1166,.T.);
#20000=ADVANCED_FACE('',(#2143),#18996,.T.);
#20001=ADVANCED_FACE('',(#2144),#1167,.T.);
#20002=ADVANCED_FACE('',(#2145),#18997,.T.);
#20003=ADVANCED_FACE('',(#2146,#689),#18998,.T.);
#20004=ADVANCED_FACE('',(#2147),#18999,.T.);
#20005=ADVANCED_FACE('',(#2148),#19000,.F.);
#20006=ADVANCED_FACE('',(#2149,#690),#19001,.F.);
#20007=ADVANCED_FACE('',(#2150),#19002,.F.);
#20008=ADVANCED_FACE('',(#2151,#691,#692,#693,#694,#695,#696,#697,#698),
#19003,.F.);
#20009=ADVANCED_FACE('',(#2152,#699,#700,#701,#702,#703,#704,#705,#706),
#19004,.F.);
#20010=ADVANCED_FACE('',(#2153),#19005,.T.);
#20011=ADVANCED_FACE('',(#2154),#19006,.T.);
#20012=ADVANCED_FACE('',(#2155),#19007,.T.);
#20013=ADVANCED_FACE('',(#2156),#19008,.T.);
#20014=ADVANCED_FACE('',(#2157,#707,#708,#709,#710,#711,#712,#713,#714,
#715,#716,#717,#718,#719,#720,#721,#722),#19009,.T.);
#20128=CLOSED_SHELL('',(#19981,#19982,#19983,#19984,#19985,#19986,#19987,
#19988,#19989,#19990,#19991,#19992,#19993,#19994,#19995,#19996,#19997,#19998,
#19999,#20000,#20001,#20002,#20003,#20004,#20005,#20006,#20007,#20008,#20009,
#20010,#20011,#20012,#20013,#20014));
#21663=AXIS2_PLACEMENT_3D('',#47627,#26395,#26396);
#21664=AXIS2_PLACEMENT_3D('',#47628,#26397,#26398);
#21665=AXIS2_PLACEMENT_3D('',#47631,#26399,#26400);
#21666=AXIS2_PLACEMENT_3D('',#47635,#26402,#26403);
#21667=AXIS2_PLACEMENT_3D('',#47642,#26407,#26408);
#21668=AXIS2_PLACEMENT_3D('',#47643,#26409,#26410);
#21669=AXIS2_PLACEMENT_3D('',#47645,#26411,#26412);
#21670=AXIS2_PLACEMENT_3D('',#47648,#26414,#26415);
#21671=AXIS2_PLACEMENT_3D('',#47649,#26416,#26417);
#21672=AXIS2_PLACEMENT_3D('',#47651,#26418,#26419);
#21673=AXIS2_PLACEMENT_3D('',#47654,#26421,#26422);
#21674=AXIS2_PLACEMENT_3D('',#47655,#26423,#26424);
#21675=AXIS2_PLACEMENT_3D('',#47657,#26425,#26426);
#21676=AXIS2_PLACEMENT_3D('',#47660,#26428,#26429);
#21677=AXIS2_PLACEMENT_3D('',#47661,#26430,#26431);
#21678=AXIS2_PLACEMENT_3D('',#47663,#26432,#26433);
#21679=AXIS2_PLACEMENT_3D('',#47666,#26435,#26436);
#21680=AXIS2_PLACEMENT_3D('',#47667,#26437,#26438);
#21681=AXIS2_PLACEMENT_3D('',#47669,#26439,#26440);
#21682=AXIS2_PLACEMENT_3D('',#47672,#26442,#26443);
#21683=AXIS2_PLACEMENT_3D('',#47673,#26444,#26445);
#21684=AXIS2_PLACEMENT_3D('',#47675,#26446,#26447);
#21685=AXIS2_PLACEMENT_3D('',#47678,#26449,#26450);
#21686=AXIS2_PLACEMENT_3D('',#47679,#26451,#26452);
#21687=AXIS2_PLACEMENT_3D('',#47681,#26453,#26454);
#21688=AXIS2_PLACEMENT_3D('',#47684,#26456,#26457);
#21689=AXIS2_PLACEMENT_3D('',#47685,#26458,#26459);
#21690=AXIS2_PLACEMENT_3D('',#47687,#26460,#26461);
#21691=AXIS2_PLACEMENT_3D('',#47690,#26463,#26464);
#21692=AXIS2_PLACEMENT_3D('',#47691,#26465,#26466);
#21693=AXIS2_PLACEMENT_3D('',#47693,#26467,#26468);
#21694=AXIS2_PLACEMENT_3D('',#47696,#26470,#26471);
#21695=AXIS2_PLACEMENT_3D('',#47697,#26472,#26473);
#21696=AXIS2_PLACEMENT_3D('',#47699,#26474,#26475);
#21697=AXIS2_PLACEMENT_3D('',#47702,#26477,#26478);
#21698=AXIS2_PLACEMENT_3D('',#47703,#26479,#26480);
#21699=AXIS2_PLACEMENT_3D('',#47705,#26481,#26482);
#21700=AXIS2_PLACEMENT_3D('',#47708,#26484,#26485);
#21701=AXIS2_PLACEMENT_3D('',#47709,#26486,#26487);
#21702=AXIS2_PLACEMENT_3D('',#47711,#26488,#26489);
#21703=AXIS2_PLACEMENT_3D('',#47714,#26491,#26492);
#21704=AXIS2_PLACEMENT_3D('',#47715,#26493,#26494);
#21705=AXIS2_PLACEMENT_3D('',#47717,#26495,#26496);
#21706=AXIS2_PLACEMENT_3D('',#47720,#26498,#26499);
#21707=AXIS2_PLACEMENT_3D('',#47721,#26500,#26501);
#21708=AXIS2_PLACEMENT_3D('',#47723,#26502,#26503);
#21709=AXIS2_PLACEMENT_3D('',#47726,#26505,#26506);
#21710=AXIS2_PLACEMENT_3D('',#47727,#26507,#26508);
#21711=AXIS2_PLACEMENT_3D('',#47729,#26509,#26510);
#21712=AXIS2_PLACEMENT_3D('',#47732,#26512,#26513);
#21713=AXIS2_PLACEMENT_3D('',#47733,#26514,#26515);
#21714=AXIS2_PLACEMENT_3D('',#47735,#26516,#26517);
#21715=AXIS2_PLACEMENT_3D('',#47738,#26519,#26520);
#21716=AXIS2_PLACEMENT_3D('',#47739,#26521,#26522);
#21717=AXIS2_PLACEMENT_3D('',#47741,#26523,#26524);
#21718=AXIS2_PLACEMENT_3D('',#47743,#26526,#26527);
#21719=AXIS2_PLACEMENT_3D('',#47746,#26528,#26529);
#21720=AXIS2_PLACEMENT_3D('',#47749,#26532,#26533);
#21721=AXIS2_PLACEMENT_3D('',#47753,#26536,#26537);
#21722=AXIS2_PLACEMENT_3D('',#47755,#26538,#26539);
#21723=AXIS2_PLACEMENT_3D('',#47757,#26541,#26542);
#21724=AXIS2_PLACEMENT_3D('',#47761,#26545,#26546);
#21725=AXIS2_PLACEMENT_3D('',#47765,#26549,#26550);
#21726=AXIS2_PLACEMENT_3D('',#47767,#26552,#26553);
#21727=AXIS2_PLACEMENT_3D('',#47776,#26558,#26559);
#21728=AXIS2_PLACEMENT_3D('',#47782,#26563,#26564);
#21729=AXIS2_PLACEMENT_3D('',#47788,#26568,#26569);
#21730=AXIS2_PLACEMENT_3D('',#47794,#26573,#26574);
#21731=AXIS2_PLACEMENT_3D('',#47800,#26578,#26579);
#21732=AXIS2_PLACEMENT_3D('',#47806,#26583,#26584);
#21733=AXIS2_PLACEMENT_3D('',#47812,#26588,#26589);
#21734=AXIS2_PLACEMENT_3D('',#47814,#26591,#26592);
#21735=AXIS2_PLACEMENT_3D('',#47816,#26594,#26595);
#26395=DIRECTION('axis',(0.,0.,1.));
#26396=DIRECTION('refdir',(1.,0.,0.));
#26397=DIRECTION('center_axis',(0.,1.,0.));
#26398=DIRECTION('ref_axis',(1.,0.,0.));
#26399=DIRECTION('center_axis',(0.,-1.,0.));
#26400=DIRECTION('ref_axis',(0.707106781186547,0.,-0.707106781186547));
#26401=DIRECTION('',(1.,0.,0.));
#26402=DIRECTION('center_axis',(0.,-1.,0.));
#26403=DIRECTION('ref_axis',(-0.707106781186547,0.,-0.707106781186547));
#26404=DIRECTION('',(0.,0.,-1.));
#26405=DIRECTION('',(-1.,0.,0.));
#26406=DIRECTION('',(0.,0.,-1.));
#26407=DIRECTION('center_axis',(0.,-1.,0.));
#26408=DIRECTION('ref_axis',(1.,0.,0.));
#26409=DIRECTION('center_axis',(0.,0.,-1.));
#26410=DIRECTION('ref_axis',(-1.,0.,0.));
#26411=DIRECTION('center_axis',(0.,0.,-1.));
#26412=DIRECTION('ref_axis',(-1.,0.,0.));
#26413=DIRECTION('',(0.,0.,-1.));
#26414=DIRECTION('center_axis',(0.,0.,1.));
#26415=DIRECTION('ref_axis',(-1.,0.,0.));
#26416=DIRECTION('center_axis',(0.,0.,-1.));
#26417=DIRECTION('ref_axis',(-1.,0.,0.));
#26418=DIRECTION('center_axis',(0.,0.,-1.));
#26419=DIRECTION('ref_axis',(-1.,0.,0.));
#26420=DIRECTION('',(0.,0.,-1.));
#26421=DIRECTION('center_axis',(0.,0.,1.));
#26422=DIRECTION('ref_axis',(-1.,0.,0.));
#26423=DIRECTION('center_axis',(0.,0.,-1.));
#26424=DIRECTION('ref_axis',(-1.,0.,0.));
#26425=DIRECTION('center_axis',(0.,0.,-1.));
#26426=DIRECTION('ref_axis',(-1.,0.,0.));
#26427=DIRECTION('',(0.,0.,-1.));
#26428=DIRECTION('center_axis',(0.,0.,1.));
#26429=DIRECTION('ref_axis',(-1.,0.,0.));
#26430=DIRECTION('center_axis',(0.,0.,-1.));
#26431=DIRECTION('ref_axis',(-1.,0.,0.));
#26432=DIRECTION('center_axis',(0.,0.,-1.));
#26433=DIRECTION('ref_axis',(-1.,0.,0.));
#26434=DIRECTION('',(0.,0.,-1.));
#26435=DIRECTION('center_axis',(0.,0.,1.));
#26436=DIRECTION('ref_axis',(-1.,0.,0.));
#26437=DIRECTION('center_axis',(0.,0.,-1.));
#26438=DIRECTION('ref_axis',(-1.,0.,0.));
#26439=DIRECTION('center_axis',(0.,0.,-1.));
#26440=DIRECTION('ref_axis',(-1.,0.,0.));
#26441=DIRECTION('',(0.,0.,-1.));
#26442=DIRECTION('center_axis',(0.,0.,1.));
#26443=DIRECTION('ref_axis',(-1.,0.,0.));
#26444=DIRECTION('center_axis',(0.,0.,-1.));
#26445=DIRECTION('ref_axis',(-1.,0.,0.));
#26446=DIRECTION('center_axis',(0.,0.,-1.));
#26447=DIRECTION('ref_axis',(-1.,0.,0.));
#26448=DIRECTION('',(0.,0.,-1.));
#26449=DIRECTION('center_axis',(0.,0.,1.));
#26450=DIRECTION('ref_axis',(-1.,0.,0.));
#26451=DIRECTION('center_axis',(0.,0.,-1.));
#26452=DIRECTION('ref_axis',(-1.,0.,0.));
#26453=DIRECTION('center_axis',(0.,0.,-1.));
#26454=DIRECTION('ref_axis',(-1.,0.,0.));
#26455=DIRECTION('',(0.,0.,-1.));
#26456=DIRECTION('center_axis',(0.,0.,1.));
#26457=DIRECTION('ref_axis',(-1.,0.,0.));
#26458=DIRECTION('center_axis',(0.,0.,-1.));
#26459=DIRECTION('ref_axis',(-1.,0.,0.));
#26460=DIRECTION('center_axis',(0.,0.,-1.));
#26461=DIRECTION('ref_axis',(-1.,0.,0.));
#26462=DIRECTION('',(0.,0.,-1.));
#26463=DIRECTION('center_axis',(0.,0.,1.));
#26464=DIRECTION('ref_axis',(-1.,0.,0.));
#26465=DIRECTION('center_axis',(0.,0.,-1.));
#26466=DIRECTION('ref_axis',(-1.,0.,0.));
#26467=DIRECTION('center_axis',(0.,0.,-1.));
#26468=DIRECTION('ref_axis',(-1.,0.,0.));
#26469=DIRECTION('',(0.,0.,-1.));
#26470=DIRECTION('center_axis',(0.,0.,1.));
#26471=DIRECTION('ref_axis',(-1.,0.,0.));
#26472=DIRECTION('center_axis',(0.,0.,-1.));
#26473=DIRECTION('ref_axis',(-1.,0.,0.));
#26474=DIRECTION('center_axis',(0.,0.,-1.));
#26475=DIRECTION('ref_axis',(-1.,0.,0.));
#26476=DIRECTION('',(0.,0.,-1.));
#26477=DIRECTION('center_axis',(0.,0.,1.));
#26478=DIRECTION('ref_axis',(-1.,0.,0.));
#26479=DIRECTION('center_axis',(0.,0.,-1.));
#26480=DIRECTION('ref_axis',(-1.,0.,0.));
#26481=DIRECTION('center_axis',(0.,0.,-1.));
#26482=DIRECTION('ref_axis',(-1.,0.,0.));
#26483=DIRECTION('',(0.,0.,-1.));
#26484=DIRECTION('center_axis',(0.,0.,1.));
#26485=DIRECTION('ref_axis',(-1.,0.,0.));
#26486=DIRECTION('center_axis',(0.,0.,-1.));
#26487=DIRECTION('ref_axis',(-1.,0.,0.));
#26488=DIRECTION('center_axis',(0.,0.,-1.));
#26489=DIRECTION('ref_axis',(-1.,0.,0.));
#26490=DIRECTION('',(0.,0.,-1.));
#26491=DIRECTION('center_axis',(0.,0.,1.));
#26492=DIRECTION('ref_axis',(-1.,0.,0.));
#26493=DIRECTION('center_axis',(0.,0.,-1.));
#26494=DIRECTION('ref_axis',(-1.,0.,0.));
#26495=DIRECTION('center_axis',(0.,0.,-1.));
#26496=DIRECTION('ref_axis',(-1.,0.,0.));
#26497=DIRECTION('',(0.,0.,-1.));
#26498=DIRECTION('center_axis',(0.,0.,1.));
#26499=DIRECTION('ref_axis',(-1.,0.,0.));
#26500=DIRECTION('center_axis',(0.,0.,-1.));
#26501=DIRECTION('ref_axis',(-1.,0.,0.));
#26502=DIRECTION('center_axis',(0.,0.,-1.));
#26503=DIRECTION('ref_axis',(-1.,0.,0.));
#26504=DIRECTION('',(0.,0.,-1.));
#26505=DIRECTION('center_axis',(0.,0.,1.));
#26506=DIRECTION('ref_axis',(-1.,0.,0.));
#26507=DIRECTION('center_axis',(0.,0.,-1.));
#26508=DIRECTION('ref_axis',(-1.,0.,0.));
#26509=DIRECTION('center_axis',(0.,0.,-1.));
#26510=DIRECTION('ref_axis',(-1.,0.,0.));
#26511=DIRECTION('',(0.,0.,-1.));
#26512=DIRECTION('center_axis',(0.,0.,1.));
#26513=DIRECTION('ref_axis',(-1.,0.,0.));
#26514=DIRECTION('center_axis',(0.,0.,-1.));
#26515=DIRECTION('ref_axis',(-1.,0.,0.));
#26516=DIRECTION('center_axis',(0.,0.,-1.));
#26517=DIRECTION('ref_axis',(-1.,0.,0.));
#26518=DIRECTION('',(0.,0.,-1.));
#26519=DIRECTION('center_axis',(0.,0.,1.));
#26520=DIRECTION('ref_axis',(-1.,0.,0.));
#26521=DIRECTION('center_axis',(0.,1.,0.));
#26522=DIRECTION('ref_axis',(1.,0.,0.));
#26523=DIRECTION('center_axis',(0.,1.,0.));
#26524=DIRECTION('ref_axis',(1.,0.,0.));
#26525=DIRECTION('',(1.22464679914735E-16,1.,-1.49975978266186E-32));
#26526=DIRECTION('center_axis',(0.,-1.,0.));
#26527=DIRECTION('ref_axis',(0.707106781186547,0.,-0.707106781186547));
#26528=DIRECTION('center_axis',(0.,1.,0.));
#26529=DIRECTION('ref_axis',(0.707106781186547,0.,-0.707106781186547));
#26530=DIRECTION('',(0.,1.,0.));
#26531=DIRECTION('',(0.,-1.,0.));
#26532=DIRECTION('center_axis',(0.,0.,-1.));
#26533=DIRECTION('ref_axis',(-1.,0.,0.));
#26534=DIRECTION('',(-1.,0.,0.));
#26535=DIRECTION('',(0.,-1.,0.));
#26536=DIRECTION('center_axis',(0.,1.,0.));
#26537=DIRECTION('ref_axis',(-0.707106781186547,0.,-0.707106781186547));
#26538=DIRECTION('center_axis',(0.,1.,0.));
#26539=DIRECTION('ref_axis',(-0.707106781186547,0.,-0.707106781186547));
#26540=DIRECTION('',(0.,1.,0.));
#26541=DIRECTION('center_axis',(-1.,0.,0.));
#26542=DIRECTION('ref_axis',(0.,1.,0.));
#26543=DIRECTION('',(0.,0.,-1.));
#26544=DIRECTION('',(0.,-1.,0.));
#26545=DIRECTION('center_axis',(0.,-1.,0.));
#26546=DIRECTION('ref_axis',(-1.,0.,0.));
#26547=DIRECTION('',(0.,0.,-1.));
#26548=DIRECTION('',(1.,0.,0.));
#26549=DIRECTION('center_axis',(1.,0.,0.));
#26550=DIRECTION('ref_axis',(0.,-1.,0.));
#26551=DIRECTION('',(0.,1.,0.));
#26552=DIRECTION('center_axis',(1.,0.,0.));
#26553=DIRECTION('ref_axis',(0.,0.,-1.));
#26554=DIRECTION('',(0.,0.,-1.));
#26555=DIRECTION('',(0.,1.,0.));
#26556=DIRECTION('',(0.,0.,1.));
#26557=DIRECTION('',(0.,1.,0.));
#26558=DIRECTION('center_axis',(0.,0.,1.));
#26559=DIRECTION('ref_axis',(1.,0.,0.));
#26560=DIRECTION('',(1.,0.,0.));
#26561=DIRECTION('',(0.,1.,0.));
#26562=DIRECTION('',(-1.,0.,0.));
#26563=DIRECTION('center_axis',(-1.,0.,0.));
#26564=DIRECTION('ref_axis',(0.,0.,1.));
#26565=DIRECTION('',(0.,0.,1.));
#26566=DIRECTION('',(0.,-1.,0.));
#26567=DIRECTION('',(0.,0.,-1.));
#26568=DIRECTION('center_axis',(0.,0.,1.));
#26569=DIRECTION('ref_axis',(1.,0.,0.));
#26570=DIRECTION('',(-1.,0.,0.));
#26571=DIRECTION('',(0.,1.,0.));
#26572=DIRECTION('',(1.,0.,0.));
#26573=DIRECTION('center_axis',(0.,0.,1.));
#26574=DIRECTION('ref_axis',(1.,0.,0.));
#26575=DIRECTION('',(1.,0.,0.));
#26576=DIRECTION('',(0.,-1.,0.));
#26577=DIRECTION('',(-1.,0.,0.));
#26578=DIRECTION('center_axis',(0.,-1.,0.));
#26579=DIRECTION('ref_axis',(1.,0.,0.));
#26580=DIRECTION('',(0.,0.,1.));
#26581=DIRECTION('',(1.,0.,0.));
#26582=DIRECTION('',(0.,0.,1.));
#26583=DIRECTION('center_axis',(0.,1.,0.));
#26584=DIRECTION('ref_axis',(-1.,0.,0.));
#26585=DIRECTION('',(0.,0.,1.));
#26586=DIRECTION('',(-1.,0.,0.));
#26587=DIRECTION('',(0.,0.,1.));
#26588=DIRECTION('center_axis',(1.,0.,0.));
#26589=DIRECTION('ref_axis',(0.,1.,0.));
#26590=DIRECTION('',(0.,1.,0.));
#26591=DIRECTION('center_axis',(-1.,0.,0.));
#26592=DIRECTION('ref_axis',(0.,-1.,0.));
#26593=DIRECTION('',(0.,-1.,0.));
#26594=DIRECTION('center_axis',(0.,0.,1.));
#26595=DIRECTION('ref_axis',(1.,0.,0.));
#47627=CARTESIAN_POINT('',(0.,0.,0.));
#47628=CARTESIAN_POINT('Origin',(54.380525740571,212.,66.9996518063507));
#47629=CARTESIAN_POINT('',(90.6194742594292,212.,37.9996518063507));
#47630=CARTESIAN_POINT('',(95.6194742594292,212.,42.9996518063507));
#47631=CARTESIAN_POINT('Origin',(90.6194742594292,212.,42.9996518063507));
#47632=CARTESIAN_POINT('',(59.380525740571,212.,37.9996518063507));
#47633=CARTESIAN_POINT('',(54.380525740571,212.,37.9996518063507));
#47634=CARTESIAN_POINT('',(54.380525740571,212.,42.9996518063507));
#47635=CARTESIAN_POINT('Origin',(59.380525740571,212.,42.9996518063507));
#47636=CARTESIAN_POINT('',(54.380525740571,212.,66.9996518063507));
#47637=CARTESIAN_POINT('',(54.380525740571,212.,66.9996518063507));
#47638=CARTESIAN_POINT('',(95.6194742594292,212.,66.9996518063507));
#47639=CARTESIAN_POINT('',(45.7696402469604,212.,66.9996518063507));
#47640=CARTESIAN_POINT('',(95.6194742594292,212.,66.9996518063507));
#47641=CARTESIAN_POINT('',(66.8941998948689,212.,53.0228109606356));
#47642=CARTESIAN_POINT('Origin',(74.9879498948689,212.,53.0228109606356));
#47643=CARTESIAN_POINT('Origin',(118.97074981153,135.774646529765,79.9996518063507));
#47644=CARTESIAN_POINT('',(121.97074981153,135.774646529765,79.9996518063507));
#47645=CARTESIAN_POINT('Origin',(118.97074981153,135.774646529765,79.9996518063507));
#47646=CARTESIAN_POINT('',(121.97074981153,135.774646529765,59.9996518063507));
#47647=CARTESIAN_POINT('',(121.97074981153,135.774646529765,79.9996518063507));
#47648=CARTESIAN_POINT('Origin',(118.97074981153,135.774646529765,59.9996518063507));
#47649=CARTESIAN_POINT('Origin',(150.97074981153,273.774646529765,79.9996518063507));
#47650=CARTESIAN_POINT('',(153.97074981153,273.774646529765,79.9996518063507));
#47651=CARTESIAN_POINT('Origin',(150.97074981153,273.774646529765,79.9996518063507));
#47652=CARTESIAN_POINT('',(153.97074981153,273.774646529765,59.9996518063507));
#47653=CARTESIAN_POINT('',(153.97074981153,273.774646529765,79.9996518063507));
#47654=CARTESIAN_POINT('Origin',(150.97074981153,273.774646529765,59.9996518063507));
#47655=CARTESIAN_POINT('Origin',(-1.02925018847036,273.774646529765,79.9996518063507));
#47656=CARTESIAN_POINT('',(1.97074981152964,273.774646529765,79.9996518063507));
#47657=CARTESIAN_POINT('Origin',(-1.02925018847036,273.774646529765,79.9996518063507));
#47658=CARTESIAN_POINT('',(1.97074981152964,273.774646529765,59.9996518063507));
#47659=CARTESIAN_POINT('',(1.97074981152964,273.774646529765,79.9996518063507));
#47660=CARTESIAN_POINT('Origin',(-1.02925018847036,273.774646529765,59.9996518063507));
#47661=CARTESIAN_POINT('Origin',(-1.02925018847036,171.774646529765,79.9996518063507));
#47662=CARTESIAN_POINT('',(1.97074981152964,171.774646529765,79.9996518063507));
#47663=CARTESIAN_POINT('Origin',(-1.02925018847036,171.774646529765,79.9996518063507));
#47664=CARTESIAN_POINT('',(1.97074981152964,171.774646529765,59.9996518063507));
#47665=CARTESIAN_POINT('',(1.97074981152964,171.774646529765,79.9996518063507));
#47666=CARTESIAN_POINT('Origin',(-1.02925018847036,171.774646529765,59.9996518063507));
#47667=CARTESIAN_POINT('Origin',(30.9707498115296,135.774646529765,79.9996518063507));
#47668=CARTESIAN_POINT('',(33.9707498115296,135.774646529765,79.9996518063507));
#47669=CARTESIAN_POINT('Origin',(30.9707498115296,135.774646529765,79.9996518063507));
#47670=CARTESIAN_POINT('',(33.9707498115296,135.774646529765,59.9996518063507));
#47671=CARTESIAN_POINT('',(33.9707498115296,135.774646529765,79.9996518063507));
#47672=CARTESIAN_POINT('Origin',(30.9707498115296,135.774646529765,59.9996518063507));
#47673=CARTESIAN_POINT('Origin',(30.9707498115296,237.774646529765,79.9996518063507));
#47674=CARTESIAN_POINT('',(33.9707498115296,237.774646529765,79.9996518063507));
#47675=CARTESIAN_POINT('Origin',(30.9707498115296,237.774646529765,79.9996518063507));
#47676=CARTESIAN_POINT('',(33.9707498115296,237.774646529765,59.9996518063507));
#47677=CARTESIAN_POINT('',(33.9707498115296,237.774646529765,79.9996518063507));
#47678=CARTESIAN_POINT('Origin',(30.9707498115296,237.774646529765,59.9996518063507));
#47679=CARTESIAN_POINT('Origin',(118.97074981153,273.774646529765,79.9996518063507));
#47680=CARTESIAN_POINT('',(121.97074981153,273.774646529765,79.9996518063507));
#47681=CARTESIAN_POINT('Origin',(118.97074981153,273.774646529765,79.9996518063507));
#47682=CARTESIAN_POINT('',(121.97074981153,273.774646529765,59.9996518063507));
#47683=CARTESIAN_POINT('',(121.97074981153,273.774646529765,79.9996518063507));
#47684=CARTESIAN_POINT('Origin',(118.97074981153,273.774646529765,59.9996518063507));
#47685=CARTESIAN_POINT('Origin',(118.97074981153,171.774646529765,79.9996518063507));
#47686=CARTESIAN_POINT('',(121.97074981153,171.774646529765,79.9996518063507));
#47687=CARTESIAN_POINT('Origin',(118.97074981153,171.774646529765,79.9996518063507));
#47688=CARTESIAN_POINT('',(121.97074981153,171.774646529765,59.9996518063507));
#47689=CARTESIAN_POINT('',(121.97074981153,171.774646529765,79.9996518063507));
#47690=CARTESIAN_POINT('Origin',(118.97074981153,171.774646529765,59.9996518063507));
#47691=CARTESIAN_POINT('Origin',(150.97074981153,171.774646529765,79.9996518063507));
#47692=CARTESIAN_POINT('',(153.97074981153,171.774646529765,79.9996518063507));
#47693=CARTESIAN_POINT('Origin',(150.97074981153,171.774646529765,79.9996518063507));
#47694=CARTESIAN_POINT('',(153.97074981153,171.774646529765,59.9996518063507));
#47695=CARTESIAN_POINT('',(153.97074981153,171.774646529765,79.9996518063507));
#47696=CARTESIAN_POINT('Origin',(150.97074981153,171.774646529765,59.9996518063507));
#47697=CARTESIAN_POINT('Origin',(118.97074981153,237.774646529765,79.9996518063507));
#47698=CARTESIAN_POINT('',(121.97074981153,237.774646529765,79.9996518063507));
#47699=CARTESIAN_POINT('Origin',(118.97074981153,237.774646529765,79.9996518063507));
#47700=CARTESIAN_POINT('',(121.97074981153,237.774646529765,59.9996518063507));
#47701=CARTESIAN_POINT('',(121.97074981153,237.774646529765,79.9996518063507));
#47702=CARTESIAN_POINT('Origin',(118.97074981153,237.774646529765,59.9996518063507));
#47703=CARTESIAN_POINT('Origin',(30.9707498115296,273.774646529765,79.9996518063507));
#47704=CARTESIAN_POINT('',(33.9707498115296,273.774646529765,79.9996518063507));
#47705=CARTESIAN_POINT('Origin',(30.9707498115296,273.774646529765,79.9996518063507));
#47706=CARTESIAN_POINT('',(33.9707498115296,273.774646529765,59.9996518063507));
#47707=CARTESIAN_POINT('',(33.9707498115296,273.774646529765,79.9996518063507));
#47708=CARTESIAN_POINT('Origin',(30.9707498115296,273.774646529765,59.9996518063507));
#47709=CARTESIAN_POINT('Origin',(-1.02925018847036,135.774646529765,79.9996518063507));
#47710=CARTESIAN_POINT('',(1.97074981152964,135.774646529765,79.9996518063507));
#47711=CARTESIAN_POINT('Origin',(-1.02925018847036,135.774646529765,79.9996518063507));
#47712=CARTESIAN_POINT('',(1.97074981152964,135.774646529765,59.9996518063507));
#47713=CARTESIAN_POINT('',(1.97074981152964,135.774646529765,79.9996518063507));
#47714=CARTESIAN_POINT('Origin',(-1.02925018847036,135.774646529765,59.9996518063507));
#47715=CARTESIAN_POINT('Origin',(30.9707498115296,171.774646529765,79.9996518063507));
#47716=CARTESIAN_POINT('',(33.9707498115296,171.774646529765,79.9996518063507));
#47717=CARTESIAN_POINT('Origin',(30.9707498115296,171.774646529765,79.9996518063507));
#47718=CARTESIAN_POINT('',(33.9707498115296,171.774646529765,59.9996518063507));
#47719=CARTESIAN_POINT('',(33.9707498115296,171.774646529765,79.9996518063507));
#47720=CARTESIAN_POINT('Origin',(30.9707498115296,171.774646529765,59.9996518063507));
#47721=CARTESIAN_POINT('Origin',(-1.02925018847036,237.774646529765,79.9996518063507));
#47722=CARTESIAN_POINT('',(1.97074981152964,237.774646529765,79.9996518063507));
#47723=CARTESIAN_POINT('Origin',(-1.02925018847036,237.774646529765,79.9996518063507));
#47724=CARTESIAN_POINT('',(1.97074981152964,237.774646529765,59.9996518063507));
#47725=CARTESIAN_POINT('',(1.97074981152964,237.774646529765,79.9996518063507));
#47726=CARTESIAN_POINT('Origin',(-1.02925018847036,237.774646529765,59.9996518063507));
#47727=CARTESIAN_POINT('Origin',(150.97074981153,237.774646529765,79.9996518063507));
#47728=CARTESIAN_POINT('',(153.97074981153,237.774646529765,79.9996518063507));
#47729=CARTESIAN_POINT('Origin',(150.97074981153,237.774646529765,79.9996518063507));
#47730=CARTESIAN_POINT('',(153.97074981153,237.774646529765,59.9996518063507));
#47731=CARTESIAN_POINT('',(153.97074981153,237.774646529765,79.9996518063507));
#47732=CARTESIAN_POINT('Origin',(150.97074981153,237.774646529765,59.9996518063507));
#47733=CARTESIAN_POINT('Origin',(150.97074981153,135.774646529765,79.9996518063507));
#47734=CARTESIAN_POINT('',(153.97074981153,135.774646529765,79.9996518063507));
#47735=CARTESIAN_POINT('Origin',(150.97074981153,135.774646529765,79.9996518063507));
#47736=CARTESIAN_POINT('',(153.97074981153,135.774646529765,59.9996518063507));
#47737=CARTESIAN_POINT('',(153.97074981153,135.774646529765,79.9996518063507));
#47738=CARTESIAN_POINT('Origin',(150.97074981153,135.774646529765,59.9996518063507));
#47739=CARTESIAN_POINT('Origin',(74.9879498948689,189.688844000289,53.0228109606356));
#47740=CARTESIAN_POINT('',(66.8941998948689,198.,53.0228109606356));
#47741=CARTESIAN_POINT('Origin',(74.9879498948689,198.,53.0228109606356));
#47742=CARTESIAN_POINT('',(66.8941998948689,189.688844000289,53.0228109606356));
#47743=CARTESIAN_POINT('Origin',(90.6194742594292,208.5,42.9996518063507));
#47744=CARTESIAN_POINT('',(95.6194742594292,198.,42.9996518063507));
#47745=CARTESIAN_POINT('',(90.6194742594292,198.,37.9996518063507));
#47746=CARTESIAN_POINT('Origin',(90.6194742594292,198.,42.9996518063507));
#47747=CARTESIAN_POINT('',(90.6194742594292,208.5,37.9996518063507));
#47748=CARTESIAN_POINT('',(95.6194742594292,208.5,42.9996518063507));
#47749=CARTESIAN_POINT('Origin',(75.0000000000001,205.,37.9996518063507));
#47750=CARTESIAN_POINT('',(59.380525740571,198.,37.9996518063507));
#47751=CARTESIAN_POINT('',(95.6194742594292,198.,37.9996518063507));
#47752=CARTESIAN_POINT('',(59.380525740571,201.5,37.9996518063507));
#47753=CARTESIAN_POINT('Origin',(59.380525740571,201.5,42.9996518063507));
#47754=CARTESIAN_POINT('',(54.380525740571,198.,42.9996518063507));
#47755=CARTESIAN_POINT('Origin',(59.380525740571,198.,42.9996518063507));
#47756=CARTESIAN_POINT('',(54.380525740571,201.5,42.9996518063507));
#47757=CARTESIAN_POINT('Origin',(54.380525740571,198.,66.9996518063507));
#47758=CARTESIAN_POINT('',(54.380525740571,198.,66.9996518063507));
#47759=CARTESIAN_POINT('',(54.380525740571,198.,66.9996518063507));
#47760=CARTESIAN_POINT('',(54.380525740571,157.,66.9996518063507));
#47761=CARTESIAN_POINT('Origin',(95.6194742594292,198.,66.9996518063507));
#47762=CARTESIAN_POINT('',(95.6194742594292,198.,66.9996518063507));
#47763=CARTESIAN_POINT('',(95.6194742594292,198.,66.9996518063507));
#47764=CARTESIAN_POINT('',(66.3891145063896,198.,66.9996518063507));
#47765=CARTESIAN_POINT('Origin',(95.6194742594292,212.,66.9996518063507));
#47766=CARTESIAN_POINT('',(95.6194742594292,164.,66.9996518063507));
#47767=CARTESIAN_POINT('Origin',(112.84124524665,116.,66.9996518063507));
#47768=CARTESIAN_POINT('',(112.84124524665,116.,66.9996518063507));
#47769=CARTESIAN_POINT('',(112.84124524665,116.,59.9996518063507));
#47770=CARTESIAN_POINT('',(112.84124524665,116.,63.4996518063507));
#47771=CARTESIAN_POINT('',(112.84124524665,294.,66.9996518063507));
#47772=CARTESIAN_POINT('',(112.84124524665,116.,66.9996518063507));
#47773=CARTESIAN_POINT('',(112.84124524665,294.,59.9996518063507));
#47774=CARTESIAN_POINT('',(112.84124524665,294.,63.4996518063507));
#47775=CARTESIAN_POINT('',(112.84124524665,160.5,59.9996518063507));
#47776=CARTESIAN_POINT('Origin',(37.1587547533499,116.,66.9996518063507));
#47777=CARTESIAN_POINT('',(37.1587547533499,116.,66.9996518063507));
#47778=CARTESIAN_POINT('',(15.3915723951113,116.,66.9996518063507));
#47779=CARTESIAN_POINT('',(37.1587547533499,294.,66.9996518063507));
#47780=CARTESIAN_POINT('',(37.1587547533499,116.,66.9996518063507));
#47781=CARTESIAN_POINT('',(96.7671823582386,294.,66.9996518063507));
#47782=CARTESIAN_POINT('Origin',(37.1587547533499,116.,59.9996518063507));
#47783=CARTESIAN_POINT('',(37.1587547533499,116.,59.9996518063507));
#47784=CARTESIAN_POINT('',(37.1587547533499,116.,59.9996518063507));
#47785=CARTESIAN_POINT('',(37.1587547533499,294.,59.9996518063507));
#47786=CARTESIAN_POINT('',(37.1587547533499,160.5,59.9996518063507));
#47787=CARTESIAN_POINT('',(37.1587547533499,294.,59.9996518063507));
#47788=CARTESIAN_POINT('Origin',(75.,205.,59.9996518063507));
#47789=CARTESIAN_POINT('',(156.375609963127,294.,59.9996518063507));
#47790=CARTESIAN_POINT('',(156.375609963127,294.,59.9996518063507));
#47791=CARTESIAN_POINT('',(156.375609963127,116.,59.9996518063507));
#47792=CARTESIAN_POINT('',(156.375609963127,116.,59.9996518063507));
#47793=CARTESIAN_POINT('',(-6.37560996312729,116.,59.9996518063507));
#47794=CARTESIAN_POINT('Origin',(75.,205.,59.9996518063507));
#47795=CARTESIAN_POINT('',(-6.37560996312729,116.,59.9996518063507));
#47796=CARTESIAN_POINT('',(-6.37560996312729,116.,59.9996518063507));
#47797=CARTESIAN_POINT('',(-6.37560996312729,294.,59.9996518063507));
#47798=CARTESIAN_POINT('',(-6.37560996312729,294.,59.9996518063507));
#47799=CARTESIAN_POINT('',(156.375609963127,294.,59.9996518063507));
#47800=CARTESIAN_POINT('Origin',(-6.37560996312729,116.,59.9996518063507));
#47801=CARTESIAN_POINT('',(156.375609963127,116.,79.9996518063507));
#47802=CARTESIAN_POINT('',(156.375609963127,116.,59.9996518063507));
#47803=CARTESIAN_POINT('',(-6.37560996312729,116.,79.9996518063507));
#47804=CARTESIAN_POINT('',(-6.37560996312729,116.,79.9996518063507));
#47805=CARTESIAN_POINT('',(-6.37560996312729,116.,59.9996518063507));
#47806=CARTESIAN_POINT('Origin',(156.375609963127,294.,59.9996518063507));
#47807=CARTESIAN_POINT('',(-6.37560996312729,294.,79.9996518063507));
#47808=CARTESIAN_POINT('',(-6.37560996312729,294.,59.9996518063507));
#47809=CARTESIAN_POINT('',(156.375609963127,294.,79.9996518063507));
#47810=CARTESIAN_POINT('',(156.375609963127,294.,79.9996518063507));
#47811=CARTESIAN_POINT('',(156.375609963127,294.,59.9996518063507));
#47812=CARTESIAN_POINT('Origin',(156.375609963127,116.,59.9996518063507));
#47813=CARTESIAN_POINT('',(156.375609963127,116.,79.9996518063507));
#47814=CARTESIAN_POINT('Origin',(-6.37560996312729,294.,59.9996518063507));
#47815=CARTESIAN_POINT('',(-6.37560996312729,294.,79.9996518063507));
#47816=CARTESIAN_POINT('Origin',(75.,205.,79.9996518063507));
#48350=UNCERTAINTY_MEASURE_WITH_UNIT(LENGTH_MEASURE(0.01),#48370,
'DISTANCE_ACCURACY_VALUE',
'Maximum model space distance between geometric entities at asserted c
onnectivities');
#48356=UNCERTAINTY_MEASURE_WITH_UNIT(LENGTH_MEASURE(0.01),#48370,
'DISTANCE_ACCURACY_VALUE',
'Maximum model space distance between geometric entities at asserted c
onnectivities');
#48363=(
GEOMETRIC_REPRESENTATION_CONTEXT(3)
GLOBAL_UNCERTAINTY_ASSIGNED_CONTEXT((#48350))
GLOBAL_UNIT_ASSIGNED_CONTEXT((#48370,#48372,#48373))
REPRESENTATION_CONTEXT('','3D')
);
#48369=(
GEOMETRIC_REPRESENTATION_CONTEXT(3)
GLOBAL_UNCERTAINTY_ASSIGNED_CONTEXT((#48356))
GLOBAL_UNIT_ASSIGNED_CONTEXT((#48370,#48372,#48373))
REPRESENTATION_CONTEXT('','3D')
);
#48370=(
LENGTH_UNIT()
NAMED_UNIT(*)
SI_UNIT(.MILLI.,.METRE.)
);
#48372=(
NAMED_UNIT(*)
PLANE_ANGLE_UNIT()
SI_UNIT($,.RADIAN.)
);
#48373=(
NAMED_UNIT(*)
SI_UNIT($,.STERADIAN.)
SOLID_ANGLE_UNIT()
);
#48380=SHAPE_DEFINITION_REPRESENTATION(#48392,#48418);
#48392=PRODUCT_DEFINITION_SHAPE('',$,#48431);
#48418=SHAPE_REPRESENTATION('',(#21663),#48363);
#48424=PRODUCT_DEFINITION_CONTEXT('part definition',#48462,'design');
#48431=PRODUCT_DEFINITION('Middle_Block','Middle_Block',#48443,#48424);
#48443=PRODUCT_DEFINITION_FORMATION('',$,#48470);
#48462=APPLICATION_CONTEXT(
'Core Data for Automotive Mechanical Design Process');
#48463=PRODUCT_CONTEXT('part definition',#48462,'mechanical');
#48470=PRODUCT('Middle_Block','Middle_Block',$,(#48463));
#48490=COLOUR_RGB('Dark Blue',0.08,0.2,0.34);
#48491=FILL_AREA_STYLE_COLOUR('',#48490);
#48492=FILL_AREA_STYLE('',(#48491));
#48493=SURFACE_STYLE_FILL_AREA(#48492);
#48494=SURFACE_SIDE_STYLE('',(#48493));
#48495=SURFACE_STYLE_USAGE(.BOTH.,#48494);
#48496=PRESENTATION_STYLE_ASSIGNMENT((#48495));
ENDSEC;
END-ISO-10303-21;
